ISO-10303-21;
HEADER;
/* Generated by software containing ST-Developer
 * from STEP Tools, Inc. (www.steptools.com) 
 */

FILE_DESCRIPTION(
/* description */ ('Over-Centre Plunger Toggle Clamp on Slotted Fixture Frame'),
/* implementation_level */ '2;1');

FILE_NAME(
/* name */ 
'Cap Screw - M4x16.step',
/* time_stamp */ '2026-10-28T03:23:24-07:00',
/* author */ (''),
/* organization */ (''),
/* preprocessor_version */ 'ST-DEVELOPER v20.2',
/* originating_system */ 'Autodesk Translation Framework v15.17.0.0',
/* authorisation */ '');

FILE_SCHEMA (('AUTOMOTIVE_DESIGN { 1 0 10303 214 3 1 1 }'));
ENDSEC;

DATA;
#10=MECHANICAL_DESIGN_GEOMETRIC_PRESENTATION_REPRESENTATION('',(#555),#15212);
#400=ORIENTED_CLOSED_SHELL('',*,#8291,.F.);
#404=BREP_WITH_VOIDS('Body1',#8290,(#400));
#421=CONICAL_SURFACE('',#9542,0.325,0.785398163397448);
#422=CONICAL_SURFACE('',#9546,0.335,0.785398163397448);
#423=CONICAL_SURFACE('',#9550,0.21,0.463647609000806);
#424=CONICAL_SURFACE('',#9554,0.18,0.785398163397448);
#463=SHAPE_REPRESENTATION_RELATIONSHIP('SRR','None',#15440,#505);
#505=ADVANCED_BREP_SHAPE_REPRESENTATION('',(#404),#15202);
#555=STYLED_ITEM('',(#15726),#404);
#767=FACE_BOUND('',#2143,.T.);
#1035=PLANE('',#9540);
#1036=PLANE('',#9548);
#1037=PLANE('',#9556);
#1038=PLANE('',#9557);
#1039=PLANE('',#9558);
#1040=PLANE('',#9559);
#1041=PLANE('',#9560);
#1042=PLANE('',#9561);
#1043=PLANE('',#9562);
#1044=PLANE('',#9563);
#1045=PLANE('',#9564);
#1496=FACE_OUTER_BOUND('',#2138,.T.);
#1497=FACE_OUTER_BOUND('',#2139,.T.);
#1498=FACE_OUTER_BOUND('',#2140,.T.);
#1499=FACE_OUTER_BOUND('',#2141,.T.);
#1500=FACE_OUTER_BOUND('',#2142,.T.);
#1501=FACE_OUTER_BOUND('',#2144,.T.);
#1502=FACE_OUTER_BOUND('',#2145,.T.);
#1503=FACE_OUTER_BOUND('',#2146,.T.);
#1504=FACE_OUTER_BOUND('',#2147,.T.);
#1505=FACE_OUTER_BOUND('',#2148,.T.);
#1506=FACE_OUTER_BOUND('',#2149,.T.);
#1507=FACE_OUTER_BOUND('',#2150,.T.);
#1508=FACE_OUTER_BOUND('',#2151,.T.);
#1509=FACE_OUTER_BOUND('',#2152,.T.);
#1510=FACE_OUTER_BOUND('',#2153,.T.);
#1511=FACE_OUTER_BOUND('',#2154,.T.);
#1512=FACE_OUTER_BOUND('',#2155,.T.);
#2138=EDGE_LOOP('',(#7313));
#2139=EDGE_LOOP('',(#7314,#7315,#7316,#7317));
#2140=EDGE_LOOP('',(#7318,#7319,#7320,#7321));
#2141=EDGE_LOOP('',(#7322,#7323,#7324,#7325));
#2142=EDGE_LOOP('',(#7326));
#2143=EDGE_LOOP('',(#7327));
#2144=EDGE_LOOP('',(#7328,#7329,#7330,#7331));
#2145=EDGE_LOOP('',(#7332,#7333,#7334,#7335));
#2146=EDGE_LOOP('',(#7336,#7337,#7338,#7339));
#2147=EDGE_LOOP('',(#7340));
#2148=EDGE_LOOP('',(#7341,#7342,#7343,#7344));
#2149=EDGE_LOOP('',(#7345,#7346,#7347,#7348));
#2150=EDGE_LOOP('',(#7349,#7350,#7351,#7352));
#2151=EDGE_LOOP('',(#7353,#7354,#7355,#7356));
#2152=EDGE_LOOP('',(#7357,#7358,#7359,#7360));
#2153=EDGE_LOOP('',(#7361,#7362,#7363,#7364));
#2154=EDGE_LOOP('',(#7365,#7366,#7367,#7368,#7369,#7370));
#2155=EDGE_LOOP('',(#7371,#7372,#7373,#7374,#7375,#7376));
#2760=LINE('',#14685,#3390);
#2761=LINE('',#14689,#3391);
#2762=LINE('',#14693,#3392);
#2763=LINE('',#14700,#3393);
#2764=LINE('',#14704,#3394);
#2765=LINE('',#14708,#3395);
#2766=LINE('',#14713,#3396);
#2767=LINE('',#14715,#3397);
#2768=LINE('',#14717,#3398);
#2769=LINE('',#14718,#3399);
#2770=LINE('',#14721,#3400);
#2771=LINE('',#14723,#3401);
#2772=LINE('',#14724,#3402);
#2773=LINE('',#14727,#3403);
#2774=LINE('',#14729,#3404);
#2775=LINE('',#14730,#3405);
#2776=LINE('',#14733,#3406);
#2777=LINE('',#14735,#3407);
#2778=LINE('',#14736,#3408);
#2779=LINE('',#14739,#3409);
#2780=LINE('',#14741,#3410);
#2781=LINE('',#14742,#3411);
#2782=LINE('',#14744,#3412);
#2783=LINE('',#14745,#3413);
#3390=VECTOR('',#11845,0.325);
#3391=VECTOR('',#11850,0.35);
#3392=VECTOR('',#11855,0.335);
#3393=VECTOR('',#11864,0.21);
#3394=VECTOR('',#11869,0.2);
#3395=VECTOR('',#11874,0.18);
#3396=VECTOR('',#11879,1.);
#3397=VECTOR('',#11880,1.);
#3398=VECTOR('',#11881,1.);
#3399=VECTOR('',#11882,1.);
#3400=VECTOR('',#11885,1.);
#3401=VECTOR('',#11886,1.);
#3402=VECTOR('',#11887,1.);
#3403=VECTOR('',#11890,1.);
#3404=VECTOR('',#11891,1.);
#3405=VECTOR('',#11892,1.);
#3406=VECTOR('',#11895,1.);
#3407=VECTOR('',#11896,1.);
#3408=VECTOR('',#11897,1.);
#3409=VECTOR('',#11900,1.);
#3410=VECTOR('',#11901,1.);
#3411=VECTOR('',#11902,1.);
#3412=VECTOR('',#11905,1.);
#3413=VECTOR('',#11906,1.);
#3810=CIRCLE('',#9541,0.3);
#3811=CIRCLE('',#9543,0.35);
#3812=CIRCLE('',#9545,0.35);
#3813=CIRCLE('',#9547,0.32);
#3814=CIRCLE('',#9549,0.22);
#3815=CIRCLE('',#9551,0.1954);
#3816=CIRCLE('',#9553,0.1954);
#3817=CIRCLE('',#9555,0.16);
#4446=VERTEX_POINT('',#14680);
#4447=VERTEX_POINT('',#14683);
#4448=VERTEX_POINT('',#14687);
#4449=VERTEX_POINT('',#14691);
#4450=VERTEX_POINT('',#14695);
#4451=VERTEX_POINT('',#14698);
#4452=VERTEX_POINT('',#14702);
#4453=VERTEX_POINT('',#14706);
#4454=VERTEX_POINT('',#14711);
#4455=VERTEX_POINT('',#14712);
#4456=VERTEX_POINT('',#14714);
#4457=VERTEX_POINT('',#14716);
#4458=VERTEX_POINT('',#14720);
#4459=VERTEX_POINT('',#14722);
#4460=VERTEX_POINT('',#14726);
#4461=VERTEX_POINT('',#14728);
#4462=VERTEX_POINT('',#14732);
#4463=VERTEX_POINT('',#14734);
#4464=VERTEX_POINT('',#14738);
#4465=VERTEX_POINT('',#14740);
#5417=EDGE_CURVE('',#4446,#4446,#3810,.T.);
#5418=EDGE_CURVE('',#4447,#4447,#3811,.T.);
#5419=EDGE_CURVE('',#4447,#4446,#2760,.T.);
#5420=EDGE_CURVE('',#4448,#4448,#3812,.T.);
#5421=EDGE_CURVE('',#4448,#4447,#2761,.T.);
#5422=EDGE_CURVE('',#4449,#4449,#3813,.T.);
#5423=EDGE_CURVE('',#4449,#4448,#2762,.T.);
#5424=EDGE_CURVE('',#4450,#4450,#3814,.T.);
#5425=EDGE_CURVE('',#4451,#4451,#3815,.F.);
#5426=EDGE_CURVE('',#4451,#4450,#2763,.T.);
#5427=EDGE_CURVE('',#4452,#4452,#3816,.F.);
#5428=EDGE_CURVE('',#4452,#4451,#2764,.T.);
#5429=EDGE_CURVE('',#4453,#4453,#3817,.T.);
#5430=EDGE_CURVE('',#4453,#4452,#2765,.T.);
#5431=EDGE_CURVE('',#4454,#4455,#2766,.T.);
#5432=EDGE_CURVE('',#4455,#4456,#2767,.T.);
#5433=EDGE_CURVE('',#4456,#4457,#2768,.T.);
#5434=EDGE_CURVE('',#4454,#4457,#2769,.T.);
#5435=EDGE_CURVE('',#4455,#4458,#2770,.T.);
#5436=EDGE_CURVE('',#4458,#4459,#2771,.T.);
#5437=EDGE_CURVE('',#4459,#4456,#2772,.T.);
#5438=EDGE_CURVE('',#4458,#4460,#2773,.T.);
#5439=EDGE_CURVE('',#4460,#4461,#2774,.T.);
#5440=EDGE_CURVE('',#4461,#4459,#2775,.T.);
#5441=EDGE_CURVE('',#4460,#4462,#2776,.T.);
#5442=EDGE_CURVE('',#4462,#4463,#2777,.T.);
#5443=EDGE_CURVE('',#4463,#4461,#2778,.T.);
#5444=EDGE_CURVE('',#4462,#4464,#2779,.T.);
#5445=EDGE_CURVE('',#4464,#4465,#2780,.T.);
#5446=EDGE_CURVE('',#4465,#4463,#2781,.T.);
#5447=EDGE_CURVE('',#4464,#4454,#2782,.T.);
#5448=EDGE_CURVE('',#4457,#4465,#2783,.T.);
#7313=ORIENTED_EDGE('',*,*,#5417,.F.);
#7314=ORIENTED_EDGE('',*,*,#5418,.F.);
#7315=ORIENTED_EDGE('',*,*,#5419,.T.);
#7316=ORIENTED_EDGE('',*,*,#5417,.T.);
#7317=ORIENTED_EDGE('',*,*,#5419,.F.);
#7318=ORIENTED_EDGE('',*,*,#5420,.F.);
#7319=ORIENTED_EDGE('',*,*,#5421,.T.);
#7320=ORIENTED_EDGE('',*,*,#5418,.T.);
#7321=ORIENTED_EDGE('',*,*,#5421,.F.);
#7322=ORIENTED_EDGE('',*,*,#5422,.F.);
#7323=ORIENTED_EDGE('',*,*,#5423,.T.);
#7324=ORIENTED_EDGE('',*,*,#5420,.T.);
#7325=ORIENTED_EDGE('',*,*,#5423,.F.);
#7326=ORIENTED_EDGE('',*,*,#5422,.T.);
#7327=ORIENTED_EDGE('',*,*,#5424,.F.);
#7328=ORIENTED_EDGE('',*,*,#5425,.F.);
#7329=ORIENTED_EDGE('',*,*,#5426,.T.);
#7330=ORIENTED_EDGE('',*,*,#5424,.T.);
#7331=ORIENTED_EDGE('',*,*,#5426,.F.);
#7332=ORIENTED_EDGE('',*,*,#5427,.F.);
#7333=ORIENTED_EDGE('',*,*,#5428,.T.);
#7334=ORIENTED_EDGE('',*,*,#5425,.T.);
#7335=ORIENTED_EDGE('',*,*,#5428,.F.);
#7336=ORIENTED_EDGE('',*,*,#5429,.F.);
#7337=ORIENTED_EDGE('',*,*,#5430,.T.);
#7338=ORIENTED_EDGE('',*,*,#5427,.T.);
#7339=ORIENTED_EDGE('',*,*,#5430,.F.);
#7340=ORIENTED_EDGE('',*,*,#5429,.T.);
#7341=ORIENTED_EDGE('',*,*,#5431,.T.);
#7342=ORIENTED_EDGE('',*,*,#5432,.T.);
#7343=ORIENTED_EDGE('',*,*,#5433,.T.);
#7344=ORIENTED_EDGE('',*,*,#5434,.F.);
#7345=ORIENTED_EDGE('',*,*,#5435,.T.);
#7346=ORIENTED_EDGE('',*,*,#5436,.T.);
#7347=ORIENTED_EDGE('',*,*,#5437,.T.);
#7348=ORIENTED_EDGE('',*,*,#5432,.F.);
#7349=ORIENTED_EDGE('',*,*,#5438,.T.);
#7350=ORIENTED_EDGE('',*,*,#5439,.T.);
#7351=ORIENTED_EDGE('',*,*,#5440,.T.);
#7352=ORIENTED_EDGE('',*,*,#5436,.F.);
#7353=ORIENTED_EDGE('',*,*,#5441,.T.);
#7354=ORIENTED_EDGE('',*,*,#5442,.T.);
#7355=ORIENTED_EDGE('',*,*,#5443,.T.);
#7356=ORIENTED_EDGE('',*,*,#5439,.F.);
#7357=ORIENTED_EDGE('',*,*,#5444,.T.);
#7358=ORIENTED_EDGE('',*,*,#5445,.T.);
#7359=ORIENTED_EDGE('',*,*,#5446,.T.);
#7360=ORIENTED_EDGE('',*,*,#5442,.F.);
#7361=ORIENTED_EDGE('',*,*,#5447,.T.);
#7362=ORIENTED_EDGE('',*,*,#5434,.T.);
#7363=ORIENTED_EDGE('',*,*,#5448,.T.);
#7364=ORIENTED_EDGE('',*,*,#5445,.F.);
#7365=ORIENTED_EDGE('',*,*,#5447,.F.);
#7366=ORIENTED_EDGE('',*,*,#5444,.F.);
#7367=ORIENTED_EDGE('',*,*,#5441,.F.);
#7368=ORIENTED_EDGE('',*,*,#5438,.F.);
#7369=ORIENTED_EDGE('',*,*,#5435,.F.);
#7370=ORIENTED_EDGE('',*,*,#5431,.F.);
#7371=ORIENTED_EDGE('',*,*,#5448,.F.);
#7372=ORIENTED_EDGE('',*,*,#5433,.F.);
#7373=ORIENTED_EDGE('',*,*,#5437,.F.);
#7374=ORIENTED_EDGE('',*,*,#5440,.F.);
#7375=ORIENTED_EDGE('',*,*,#5443,.F.);
#7376=ORIENTED_EDGE('',*,*,#5446,.F.);
#7740=CYLINDRICAL_SURFACE('',#9544,0.35);
#7741=CYLINDRICAL_SURFACE('',#9552,0.1954);
#8168=ADVANCED_FACE('',(#1496),#1035,.T.);
#8169=ADVANCED_FACE('',(#1497),#421,.T.);
#8170=ADVANCED_FACE('',(#1498),#7740,.T.);
#8171=ADVANCED_FACE('',(#1499),#422,.T.);
#8172=ADVANCED_FACE('',(#1500,#767),#1036,.T.);
#8173=ADVANCED_FACE('',(#1501),#423,.T.);
#8174=ADVANCED_FACE('',(#1502),#7741,.T.);
#8175=ADVANCED_FACE('',(#1503),#424,.T.);
#8176=ADVANCED_FACE('',(#1504),#1037,.T.);
#8177=ADVANCED_FACE('',(#1505),#1038,.F.);
#8178=ADVANCED_FACE('',(#1506),#1039,.F.);
#8179=ADVANCED_FACE('',(#1507),#1040,.F.);
#8180=ADVANCED_FACE('',(#1508),#1041,.F.);
#8181=ADVANCED_FACE('',(#1509),#1042,.F.);
#8182=ADVANCED_FACE('',(#1510),#1043,.F.);
#8183=ADVANCED_FACE('',(#1511),#1044,.F.);
#8184=ADVANCED_FACE('',(#1512),#1045,.F.);
#8290=CLOSED_SHELL('',(#8168,#8169,#8170,#8171,#8172,#8173,#8174,#8175,
#8176));
#8291=CLOSED_SHELL('',(#8177,#8178,#8179,#8180,#8181,#8182,#8183,#8184));
#9539=AXIS2_PLACEMENT_3D('',#14678,#11835,#11836);
#9540=AXIS2_PLACEMENT_3D('',#14679,#11837,#11838);
#9541=AXIS2_PLACEMENT_3D('',#14681,#11839,#11840);
#9542=AXIS2_PLACEMENT_3D('',#14682,#11841,#11842);
#9543=AXIS2_PLACEMENT_3D('',#14684,#11843,#11844);
#9544=AXIS2_PLACEMENT_3D('',#14686,#11846,#11847);
#9545=AXIS2_PLACEMENT_3D('',#14688,#11848,#11849);
#9546=AXIS2_PLACEMENT_3D('',#14690,#11851,#11852);
#9547=AXIS2_PLACEMENT_3D('',#14692,#11853,#11854);
#9548=AXIS2_PLACEMENT_3D('',#14694,#11856,#11857);
#9549=AXIS2_PLACEMENT_3D('',#14696,#11858,#11859);
#9550=AXIS2_PLACEMENT_3D('',#14697,#11860,#11861);
#9551=AXIS2_PLACEMENT_3D('',#14699,#11862,#11863);
#9552=AXIS2_PLACEMENT_3D('',#14701,#11865,#11866);
#9553=AXIS2_PLACEMENT_3D('',#14703,#11867,#11868);
#9554=AXIS2_PLACEMENT_3D('',#14705,#11870,#11871);
#9555=AXIS2_PLACEMENT_3D('',#14707,#11872,#11873);
#9556=AXIS2_PLACEMENT_3D('',#14709,#11875,#11876);
#9557=AXIS2_PLACEMENT_3D('',#14710,#11877,#11878);
#9558=AXIS2_PLACEMENT_3D('',#14719,#11883,#11884);
#9559=AXIS2_PLACEMENT_3D('',#14725,#11888,#11889);
#9560=AXIS2_PLACEMENT_3D('',#14731,#11893,#11894);
#9561=AXIS2_PLACEMENT_3D('',#14737,#11898,#11899);
#9562=AXIS2_PLACEMENT_3D('',#14743,#11903,#11904);
#9563=AXIS2_PLACEMENT_3D('',#14746,#11907,#11908);
#9564=AXIS2_PLACEMENT_3D('',#14747,#11909,#11910);
#11835=DIRECTION('axis',(0.,0.,1.));
#11836=DIRECTION('refdir',(1.,0.,0.));
#11837=DIRECTION('center_axis',(0.,1.,0.));
#11838=DIRECTION('ref_axis',(0.,0.,1.));
#11839=DIRECTION('center_axis',(0.,-1.,0.));
#11840=DIRECTION('ref_axis',(1.,0.,0.));
#11841=DIRECTION('center_axis',(0.,-1.,0.));
#11842=DIRECTION('ref_axis',(1.,0.,0.));
#11843=DIRECTION('center_axis',(0.,-1.,0.));
#11844=DIRECTION('ref_axis',(1.,0.,0.));
#11845=DIRECTION('',(0.707106781186547,0.707106781186548,8.65956056235493E-17));
#11846=DIRECTION('center_axis',(0.,-1.,0.));
#11847=DIRECTION('ref_axis',(1.,0.,0.));
#11848=DIRECTION('center_axis',(0.,-1.,0.));
#11849=DIRECTION('ref_axis',(1.,0.,0.));
#11850=DIRECTION('',(0.,1.,0.));
#11851=DIRECTION('center_axis',(0.,1.,0.));
#11852=DIRECTION('ref_axis',(1.,0.,0.));
#11853=DIRECTION('center_axis',(0.,-1.,0.));
#11854=DIRECTION('ref_axis',(1.,0.,0.));
#11855=DIRECTION('',(-0.707106781186547,0.707106781186548,-8.65956056235493E-17));
#11856=DIRECTION('center_axis',(0.,-1.,0.));
#11857=DIRECTION('ref_axis',(0.,0.,-1.));
#11858=DIRECTION('center_axis',(0.,-1.,0.));
#11859=DIRECTION('ref_axis',(1.,0.,0.));
#11860=DIRECTION('center_axis',(0.,1.,0.));
#11861=DIRECTION('ref_axis',(1.,0.,0.));
#11862=DIRECTION('center_axis',(0.,1.,0.));
#11863=DIRECTION('ref_axis',(1.,0.,0.));
#11864=DIRECTION('',(-0.447213595499958,0.894427190999916,-5.47678698264203E-17));
#11865=DIRECTION('center_axis',(0.,-1.,0.));
#11866=DIRECTION('ref_axis',(1.,0.,0.));
#11867=DIRECTION('center_axis',(0.,1.,0.));
#11868=DIRECTION('ref_axis',(1.,0.,0.));
#11869=DIRECTION('',(0.,1.,0.));
#11870=DIRECTION('center_axis',(0.,1.,0.));
#11871=DIRECTION('ref_axis',(1.,0.,0.));
#11872=DIRECTION('center_axis',(0.,-1.,0.));
#11873=DIRECTION('ref_axis',(1.,0.,0.));
#11874=DIRECTION('',(-0.707106781186547,0.707106781186548,-8.65956056235493E-17));
#11875=DIRECTION('center_axis',(0.,-1.,0.));
#11876=DIRECTION('ref_axis',(0.,0.,-1.));
#11877=DIRECTION('center_axis',(0.866025403784439,0.,-0.5));
#11878=DIRECTION('ref_axis',(0.5,0.,0.866025403784439));
#11879=DIRECTION('',(-0.5,0.,-0.866025403784439));
#11880=DIRECTION('',(0.,-1.,0.));
#11881=DIRECTION('',(0.5,0.,0.866025403784439));
#11882=DIRECTION('',(0.,-1.,0.));
#11883=DIRECTION('center_axis',(1.60246890531964E-16,0.,-1.));
#11884=DIRECTION('ref_axis',(1.,0.,1.60246890531964E-16));
#11885=DIRECTION('',(-1.,0.,-1.60246890531964E-16));
#11886=DIRECTION('',(0.,-1.,0.));
#11887=DIRECTION('',(1.,0.,1.60246890531964E-16));
#11888=DIRECTION('center_axis',(-0.866025403784439,0.,-0.5));
#11889=DIRECTION('ref_axis',(0.5,0.,-0.866025403784439));
#11890=DIRECTION('',(-0.5,0.,0.866025403784439));
#11891=DIRECTION('',(0.,-1.,0.));
#11892=DIRECTION('',(0.5,0.,-0.866025403784439));
#11893=DIRECTION('center_axis',(-0.866025403784439,0.,0.5));
#11894=DIRECTION('ref_axis',(-0.5,0.,-0.866025403784439));
#11895=DIRECTION('',(0.5,0.,0.866025403784439));
#11896=DIRECTION('',(0.,-1.,0.));
#11897=DIRECTION('',(-0.5,0.,-0.866025403784439));
#11898=DIRECTION('center_axis',(-1.60246890531964E-16,0.,1.));
#11899=DIRECTION('ref_axis',(-1.,0.,-1.60246890531964E-16));
#11900=DIRECTION('',(1.,0.,1.60246890531964E-16));
#11901=DIRECTION('',(0.,-1.,0.));
#11902=DIRECTION('',(-1.,0.,-1.60246890531964E-16));
#11903=DIRECTION('center_axis',(0.866025403784439,0.,0.5));
#11904=DIRECTION('ref_axis',(-0.5,0.,0.866025403784439));
#11905=DIRECTION('',(0.5,0.,-0.866025403784439));
#11906=DIRECTION('',(-0.5,0.,0.866025403784439));
#11907=DIRECTION('center_axis',(0.,1.,0.));
#11908=DIRECTION('ref_axis',(1.,0.,0.));
#11909=DIRECTION('center_axis',(0.,-1.,0.));
#11910=DIRECTION('ref_axis',(0.,0.,-1.));
#14678=CARTESIAN_POINT('',(0.,0.,0.));
#14679=CARTESIAN_POINT('Origin',(0.3,0.4,0.));
#14680=CARTESIAN_POINT('',(-0.3,0.4,-3.67394039744206E-17));
#14681=CARTESIAN_POINT('Origin',(0.,0.4,0.));
#14682=CARTESIAN_POINT('Origin',(0.,0.375,0.));
#14683=CARTESIAN_POINT('',(-0.35,0.35,-4.28626379701573E-17));
#14684=CARTESIAN_POINT('Origin',(0.,0.35,0.));
#14685=CARTESIAN_POINT('',(-0.325,0.375,-3.9801020972289E-17));
#14686=CARTESIAN_POINT('Origin',(0.,0.19,0.));
#14687=CARTESIAN_POINT('',(-0.35,0.03,-4.28626379701574E-17));
#14688=CARTESIAN_POINT('Origin',(0.,0.03,0.));
#14689=CARTESIAN_POINT('',(-0.35,0.19,-4.28626379701574E-17));
#14690=CARTESIAN_POINT('Origin',(0.,0.0149999999999999,0.));
#14691=CARTESIAN_POINT('',(-0.32,-3.29597460435593E-17,-3.91886975727153E-17));
#14692=CARTESIAN_POINT('Origin',(0.,0.,0.));
#14693=CARTESIAN_POINT('',(-0.335,0.0149999999999999,-4.10256677714363E-17));
#14694=CARTESIAN_POINT('Origin',(0.22,0.,0.));
#14695=CARTESIAN_POINT('',(-0.22,-6.93889390390723E-18,-2.69422295812418E-17));
#14696=CARTESIAN_POINT('Origin',(0.,0.,0.));
#14697=CARTESIAN_POINT('Origin',(0.,-0.02,0.));
#14698=CARTESIAN_POINT('',(-0.1954,-0.0492,2.39295984553393E-17));
#14699=CARTESIAN_POINT('Origin',(0.,-0.0492,0.));
#14700=CARTESIAN_POINT('',(-0.21,-0.02,-2.57175827820944E-17));
#14701=CARTESIAN_POINT('Origin',(0.,-0.8,0.));
#14702=CARTESIAN_POINT('',(-0.1954,-1.5646,2.39295984553393E-17));
#14703=CARTESIAN_POINT('Origin',(0.,-1.5646,0.));
#14704=CARTESIAN_POINT('',(-0.1954,-0.8,-2.39295984553393E-17));
#14705=CARTESIAN_POINT('Origin',(0.,-1.58,0.));
#14706=CARTESIAN_POINT('',(-0.16,-1.6,-1.95943487863577E-17));
#14707=CARTESIAN_POINT('Origin',(0.,-1.6,0.));
#14708=CARTESIAN_POINT('',(-0.18,-1.58,-2.20436423846524E-17));
#14709=CARTESIAN_POINT('Origin',(0.,-1.6,0.));
#14710=CARTESIAN_POINT('Origin',(0.0866025403784439,-0.4,-0.15));
#14711=CARTESIAN_POINT('',(0.173205080756888,-0.4,0.));
#14712=CARTESIAN_POINT('',(0.0866025403784439,-0.4,-0.15));
#14713=CARTESIAN_POINT('',(0.173205080756888,-0.4,0.));
#14714=CARTESIAN_POINT('',(0.0866025403784439,-0.64,-0.15));
#14715=CARTESIAN_POINT('',(0.0866025403784439,-0.4,-0.15));
#14716=CARTESIAN_POINT('',(0.173205080756888,-0.64,0.));
#14717=CARTESIAN_POINT('',(0.173205080756888,-0.64,0.));
#14718=CARTESIAN_POINT('',(0.173205080756888,-0.4,0.));
#14719=CARTESIAN_POINT('Origin',(-0.0866025403784438,-0.4,-0.15));
#14720=CARTESIAN_POINT('',(-0.0866025403784438,-0.4,-0.15));
#14721=CARTESIAN_POINT('',(0.0866025403784439,-0.4,-0.15));
#14722=CARTESIAN_POINT('',(-0.0866025403784438,-0.64,-0.15));
#14723=CARTESIAN_POINT('',(-0.0866025403784438,-0.4,-0.15));
#14724=CARTESIAN_POINT('',(0.0866025403784439,-0.64,-0.15));
#14725=CARTESIAN_POINT('Origin',(-0.173205080756888,-0.4,-2.77555756156289E-17));
#14726=CARTESIAN_POINT('',(-0.173205080756888,-0.4,-2.12115047744981E-17));
#14727=CARTESIAN_POINT('',(-0.0866025403784438,-0.4,-0.15));
#14728=CARTESIAN_POINT('',(-0.173205080756888,-0.64,-2.77555756156289E-17));
#14729=CARTESIAN_POINT('',(-0.173205080756888,-0.4,-2.12115047744981E-17));
#14730=CARTESIAN_POINT('',(-0.0866025403784438,-0.64,-0.15));
#14731=CARTESIAN_POINT('Origin',(-0.0866025403784439,-0.4,0.15));
#14732=CARTESIAN_POINT('',(-0.0866025403784439,-0.4,0.15));
#14733=CARTESIAN_POINT('',(-0.173205080756888,-0.4,-2.12115047744981E-17));
#14734=CARTESIAN_POINT('',(-0.0866025403784439,-0.64,0.15));
#14735=CARTESIAN_POINT('',(-0.0866025403784439,-0.4,0.15));
#14736=CARTESIAN_POINT('',(-0.173205080756888,-0.64,-2.12115047744981E-17));
#14737=CARTESIAN_POINT('Origin',(0.0866025403784439,-0.4,0.15));
#14738=CARTESIAN_POINT('',(0.0866025403784439,-0.4,0.15));
#14739=CARTESIAN_POINT('',(-0.0866025403784439,-0.4,0.15));
#14740=CARTESIAN_POINT('',(0.0866025403784439,-0.64,0.15));
#14741=CARTESIAN_POINT('',(0.0866025403784439,-0.4,0.15));
#14742=CARTESIAN_POINT('',(-0.0866025403784439,-0.64,0.15));
#14743=CARTESIAN_POINT('Origin',(0.173205080756888,-0.4,0.));
#14744=CARTESIAN_POINT('',(0.0866025403784439,-0.4,0.15));
#14745=CARTESIAN_POINT('',(0.0866025403784439,-0.64,0.15));
#14746=CARTESIAN_POINT('Origin',(0.,-0.4,-2.77555756156289E-17));
#14747=CARTESIAN_POINT('Origin',(0.,-0.64,-2.77555756156289E-17));
#15152=UNCERTAINTY_MEASURE_WITH_UNIT(LENGTH_MEASURE(0.001),#15213,
'DISTANCE_ACCURACY_VALUE',
'Maximum model space distance between geometric entities at asserted c
onnectivities');
#15162=UNCERTAINTY_MEASURE_WITH_UNIT(LENGTH_MEASURE(0.001),#15213,
'DISTANCE_ACCURACY_VALUE',
'Maximum model space distance between geometric entities at asserted c
onnectivities');
#15202=(
GEOMETRIC_REPRESENTATION_CONTEXT(3)
GLOBAL_UNCERTAINTY_ASSIGNED_CONTEXT((#15152))
GLOBAL_UNIT_ASSIGNED_CONTEXT((#15213,#15215,#15216))
REPRESENTATION_CONTEXT('','3D')
);
#15212=(
GEOMETRIC_REPRESENTATION_CONTEXT(3)
GLOBAL_UNCERTAINTY_ASSIGNED_CONTEXT((#15162))
GLOBAL_UNIT_ASSIGNED_CONTEXT((#15213,#15215,#15216))
REPRESENTATION_CONTEXT('','3D')
);
#15213=(
LENGTH_UNIT()
NAMED_UNIT(*)
SI_UNIT(.CENTI.,.METRE.)
);
#15215=(
NAMED_UNIT(*)
PLANE_ANGLE_UNIT()
SI_UNIT($,.RADIAN.)
);
#15216=(
NAMED_UNIT(*)
SI_UNIT($,.STERADIAN.)
SOLID_ANGLE_UNIT()
);
#15256=SHAPE_DEFINITION_REPRESENTATION(#15312,#15440);
#15312=PRODUCT_DEFINITION_SHAPE('',$,#15490);
#15440=SHAPE_REPRESENTATION('',(#9539),#15202);
#15450=PRODUCT_DEFINITION_CONTEXT('part definition',#15599,'design');
#15490=PRODUCT_DEFINITION('Cap Screw - M4x16','Cap Screw - M4x16',#15539,
#15450);
#15539=PRODUCT_DEFINITION_FORMATION('',$,#15640);
#15599=APPLICATION_CONTEXT(
'Core Data for Automotive Mechanical Design Process');
#15600=PRODUCT_CONTEXT('part definition',#15599,'mechanical');
#15640=PRODUCT('Cap Screw - M4x16','Cap Screw - M4x16',
'Cap Screw - M4x16',(#15600));
#15720=COLOUR_RGB('Black',0.12,0.14,0.17);
#15721=FILL_AREA_STYLE_COLOUR('',#15720);
#15722=FILL_AREA_STYLE('',(#15721));
#15723=SURFACE_STYLE_FILL_AREA(#15722);
#15724=SURFACE_SIDE_STYLE('',(#15723));
#15725=SURFACE_STYLE_USAGE(.BOTH.,#15724);
#15726=PRESENTATION_STYLE_ASSIGNMENT((#15725));
ENDSEC;
END-ISO-10303-21;
